ISO-10303-21;
HEADER;
/* Generated by software containing ST-Developer
 * from STEP Tools, Inc. (www.steptools.com) 
 */

FILE_DESCRIPTION(
/* description */ ('Cam-driven reciprocating slide'),
/* implementation_level */ '2;1');

FILE_NAME(
/* name */ 'Cap Screw - M4x16.step',
/* time_stamp */ '2026-10-28T03:25:20-07:00',
/* author */ (''),
/* organization */ (''),
/* preprocessor_version */ 'ST-DEVELOPER v20.2',
/* originating_system */ 'Autodesk Translation Framework v15.17.0.0',
/* authorisation */ '');

FILE_SCHEMA (('AUTOMOTIVE_DESIGN { 1 0 10303 214 3 1 1 }'));
ENDSEC;

DATA;
#10=MECHANICAL_DESIGN_GEOMETRIC_PRESENTATION_REPRESENTATION('',(#462),#13277);
#13=ORIENTED_CLOSED_SHELL('',*,#6441,.F.);
#16=BREP_WITH_VOIDS('Body1',#6440,(#13));
#326=CONICAL_SURFACE('',#7535,0.325,0.785398163397448);
#327=CONICAL_SURFACE('',#7539,0.335,0.785398163397448);
#328=CONICAL_SURFACE('',#7543,0.21,0.463647609000806);
#329=CONICAL_SURFACE('',#7547,0.18,0.785398163397448);
#381=SHAPE_REPRESENTATION_RELATIONSHIP('SRR','None',#13477,#418);
#418=ADVANCED_BREP_SHAPE_REPRESENTATION('',(#16),#13272);
#462=STYLED_ITEM('',(#13727),#16);
#666=FACE_BOUND('',#1781,.T.);
#874=PLANE('',#7533);
#875=PLANE('',#7541);
#876=PLANE('',#7549);
#877=PLANE('',#7550);
#878=PLANE('',#7551);
#879=PLANE('',#7552);
#880=PLANE('',#7553);
#881=PLANE('',#7554);
#882=PLANE('',#7555);
#883=PLANE('',#7556);
#884=PLANE('',#7557);
#1238=FACE_OUTER_BOUND('',#1776,.T.);
#1239=FACE_OUTER_BOUND('',#1777,.T.);
#1240=FACE_OUTER_BOUND('',#1778,.T.);
#1241=FACE_OUTER_BOUND('',#1779,.T.);
#1242=FACE_OUTER_BOUND('',#1780,.T.);
#1243=FACE_OUTER_BOUND('',#1782,.T.);
#1244=FACE_OUTER_BOUND('',#1783,.T.);
#1245=FACE_OUTER_BOUND('',#1784,.T.);
#1246=FACE_OUTER_BOUND('',#1785,.T.);
#1247=FACE_OUTER_BOUND('',#1786,.T.);
#1248=FACE_OUTER_BOUND('',#1787,.T.);
#1249=FACE_OUTER_BOUND('',#1788,.T.);
#1250=FACE_OUTER_BOUND('',#1789,.T.);
#1251=FACE_OUTER_BOUND('',#1790,.T.);
#1252=FACE_OUTER_BOUND('',#1791,.T.);
#1253=FACE_OUTER_BOUND('',#1792,.T.);
#1254=FACE_OUTER_BOUND('',#1793,.T.);
#1776=EDGE_LOOP('',(#5726));
#1777=EDGE_LOOP('',(#5727,#5728,#5729,#5730));
#1778=EDGE_LOOP('',(#5731,#5732,#5733,#5734));
#1779=EDGE_LOOP('',(#5735,#5736,#5737,#5738));
#1780=EDGE_LOOP('',(#5739));
#1781=EDGE_LOOP('',(#5740));
#1782=EDGE_LOOP('',(#5741,#5742,#5743,#5744));
#1783=EDGE_LOOP('',(#5745,#5746,#5747,#5748));
#1784=EDGE_LOOP('',(#5749,#5750,#5751,#5752));
#1785=EDGE_LOOP('',(#5753));
#1786=EDGE_LOOP('',(#5754,#5755,#5756,#5757));
#1787=EDGE_LOOP('',(#5758,#5759,#5760,#5761));
#1788=EDGE_LOOP('',(#5762,#5763,#5764,#5765));
#1789=EDGE_LOOP('',(#5766,#5767,#5768,#5769));
#1790=EDGE_LOOP('',(#5770,#5771,#5772,#5773));
#1791=EDGE_LOOP('',(#5774,#5775,#5776,#5777));
#1792=EDGE_LOOP('',(#5778,#5779,#5780,#5781,#5782,#5783));
#1793=EDGE_LOOP('',(#5784,#5785,#5786,#5787,#5788,#5789));
#2215=LINE('',#12949,#2654);
#2216=LINE('',#12953,#2655);
#2217=LINE('',#12957,#2656);
#2218=LINE('',#12964,#2657);
#2219=LINE('',#12968,#2658);
#2220=LINE('',#12972,#2659);
#2221=LINE('',#12977,#2660);
#2222=LINE('',#12979,#2661);
#2223=LINE('',#12981,#2662);
#2224=LINE('',#12982,#2663);
#2225=LINE('',#12985,#2664);
#2226=LINE('',#12987,#2665);
#2227=LINE('',#12988,#2666);
#2228=LINE('',#12991,#2667);
#2229=LINE('',#12993,#2668);
#2230=LINE('',#12994,#2669);
#2231=LINE('',#12997,#2670);
#2232=LINE('',#12999,#2671);
#2233=LINE('',#13000,#2672);
#2234=LINE('',#13003,#2673);
#2235=LINE('',#13005,#2674);
#2236=LINE('',#13006,#2675);
#2237=LINE('',#13008,#2676);
#2238=LINE('',#13009,#2677);
#2654=VECTOR('',#9419,0.325);
#2655=VECTOR('',#9424,0.35);
#2656=VECTOR('',#9429,0.335);
#2657=VECTOR('',#9438,0.21);
#2658=VECTOR('',#9443,0.2);
#2659=VECTOR('',#9448,0.18);
#2660=VECTOR('',#9453,1.);
#2661=VECTOR('',#9454,1.);
#2662=VECTOR('',#9455,1.);
#2663=VECTOR('',#9456,1.);
#2664=VECTOR('',#9459,1.);
#2665=VECTOR('',#9460,1.);
#2666=VECTOR('',#9461,1.);
#2667=VECTOR('',#9464,1.);
#2668=VECTOR('',#9465,1.);
#2669=VECTOR('',#9466,1.);
#2670=VECTOR('',#9469,1.);
#2671=VECTOR('',#9470,1.);
#2672=VECTOR('',#9471,1.);
#2673=VECTOR('',#9474,1.);
#2674=VECTOR('',#9475,1.);
#2675=VECTOR('',#9476,1.);
#2676=VECTOR('',#9479,1.);
#2677=VECTOR('',#9480,1.);
#3009=CIRCLE('',#7534,0.3);
#3010=CIRCLE('',#7536,0.35);
#3011=CIRCLE('',#7538,0.35);
#3012=CIRCLE('',#7540,0.32);
#3013=CIRCLE('',#7542,0.22);
#3014=CIRCLE('',#7544,0.1954);
#3015=CIRCLE('',#7546,0.1954);
#3016=CIRCLE('',#7548,0.16);
#3504=VERTEX_POINT('',#12944);
#3505=VERTEX_POINT('',#12947);
#3506=VERTEX_POINT('',#12951);
#3507=VERTEX_POINT('',#12955);
#3508=VERTEX_POINT('',#12959);
#3509=VERTEX_POINT('',#12962);
#3510=VERTEX_POINT('',#12966);
#3511=VERTEX_POINT('',#12970);
#3512=VERTEX_POINT('',#12975);
#3513=VERTEX_POINT('',#12976);
#3514=VERTEX_POINT('',#12978);
#3515=VERTEX_POINT('',#12980);
#3516=VERTEX_POINT('',#12984);
#3517=VERTEX_POINT('',#12986);
#3518=VERTEX_POINT('',#12990);
#3519=VERTEX_POINT('',#12992);
#3520=VERTEX_POINT('',#12996);
#3521=VERTEX_POINT('',#12998);
#3522=VERTEX_POINT('',#13002);
#3523=VERTEX_POINT('',#13004);
#4253=EDGE_CURVE('',#3504,#3504,#3009,.T.);
#4254=EDGE_CURVE('',#3505,#3505,#3010,.T.);
#4255=EDGE_CURVE('',#3505,#3504,#2215,.T.);
#4256=EDGE_CURVE('',#3506,#3506,#3011,.T.);
#4257=EDGE_CURVE('',#3506,#3505,#2216,.T.);
#4258=EDGE_CURVE('',#3507,#3507,#3012,.T.);
#4259=EDGE_CURVE('',#3507,#3506,#2217,.T.);
#4260=EDGE_CURVE('',#3508,#3508,#3013,.T.);
#4261=EDGE_CURVE('',#3509,#3509,#3014,.F.);
#4262=EDGE_CURVE('',#3509,#3508,#2218,.T.);
#4263=EDGE_CURVE('',#3510,#3510,#3015,.F.);
#4264=EDGE_CURVE('',#3510,#3509,#2219,.T.);
#4265=EDGE_CURVE('',#3511,#3511,#3016,.T.);
#4266=EDGE_CURVE('',#3511,#3510,#2220,.T.);
#4267=EDGE_CURVE('',#3512,#3513,#2221,.T.);
#4268=EDGE_CURVE('',#3513,#3514,#2222,.T.);
#4269=EDGE_CURVE('',#3514,#3515,#2223,.T.);
#4270=EDGE_CURVE('',#3512,#3515,#2224,.T.);
#4271=EDGE_CURVE('',#3513,#3516,#2225,.T.);
#4272=EDGE_CURVE('',#3516,#3517,#2226,.T.);
#4273=EDGE_CURVE('',#3517,#3514,#2227,.T.);
#4274=EDGE_CURVE('',#3516,#3518,#2228,.T.);
#4275=EDGE_CURVE('',#3518,#3519,#2229,.T.);
#4276=EDGE_CURVE('',#3519,#3517,#2230,.T.);
#4277=EDGE_CURVE('',#3518,#3520,#2231,.T.);
#4278=EDGE_CURVE('',#3520,#3521,#2232,.T.);
#4279=EDGE_CURVE('',#3521,#3519,#2233,.T.);
#4280=EDGE_CURVE('',#3520,#3522,#2234,.T.);
#4281=EDGE_CURVE('',#3522,#3523,#2235,.T.);
#4282=EDGE_CURVE('',#3523,#3521,#2236,.T.);
#4283=EDGE_CURVE('',#3522,#3512,#2237,.T.);
#4284=EDGE_CURVE('',#3515,#3523,#2238,.T.);
#5726=ORIENTED_EDGE('',*,*,#4253,.F.);
#5727=ORIENTED_EDGE('',*,*,#4254,.F.);
#5728=ORIENTED_EDGE('',*,*,#4255,.T.);
#5729=ORIENTED_EDGE('',*,*,#4253,.T.);
#5730=ORIENTED_EDGE('',*,*,#4255,.F.);
#5731=ORIENTED_EDGE('',*,*,#4256,.F.);
#5732=ORIENTED_EDGE('',*,*,#4257,.T.);
#5733=ORIENTED_EDGE('',*,*,#4254,.T.);
#5734=ORIENTED_EDGE('',*,*,#4257,.F.);
#5735=ORIENTED_EDGE('',*,*,#4258,.F.);
#5736=ORIENTED_EDGE('',*,*,#4259,.T.);
#5737=ORIENTED_EDGE('',*,*,#4256,.T.);
#5738=ORIENTED_EDGE('',*,*,#4259,.F.);
#5739=ORIENTED_EDGE('',*,*,#4258,.T.);
#5740=ORIENTED_EDGE('',*,*,#4260,.F.);
#5741=ORIENTED_EDGE('',*,*,#4261,.F.);
#5742=ORIENTED_EDGE('',*,*,#4262,.T.);
#5743=ORIENTED_EDGE('',*,*,#4260,.T.);
#5744=ORIENTED_EDGE('',*,*,#4262,.F.);
#5745=ORIENTED_EDGE('',*,*,#4263,.F.);
#5746=ORIENTED_EDGE('',*,*,#4264,.T.);
#5747=ORIENTED_EDGE('',*,*,#4261,.T.);
#5748=ORIENTED_EDGE('',*,*,#4264,.F.);
#5749=ORIENTED_EDGE('',*,*,#4265,.F.);
#5750=ORIENTED_EDGE('',*,*,#4266,.T.);
#5751=ORIENTED_EDGE('',*,*,#4263,.T.);
#5752=ORIENTED_EDGE('',*,*,#4266,.F.);
#5753=ORIENTED_EDGE('',*,*,#4265,.T.);
#5754=ORIENTED_EDGE('',*,*,#4267,.T.);
#5755=ORIENTED_EDGE('',*,*,#4268,.T.);
#5756=ORIENTED_EDGE('',*,*,#4269,.T.);
#5757=ORIENTED_EDGE('',*,*,#4270,.F.);
#5758=ORIENTED_EDGE('',*,*,#4271,.T.);
#5759=ORIENTED_EDGE('',*,*,#4272,.T.);
#5760=ORIENTED_EDGE('',*,*,#4273,.T.);
#5761=ORIENTED_EDGE('',*,*,#4268,.F.);
#5762=ORIENTED_EDGE('',*,*,#4274,.T.);
#5763=ORIENTED_EDGE('',*,*,#4275,.T.);
#5764=ORIENTED_EDGE('',*,*,#4276,.T.);
#5765=ORIENTED_EDGE('',*,*,#4272,.F.);
#5766=ORIENTED_EDGE('',*,*,#4277,.T.);
#5767=ORIENTED_EDGE('',*,*,#4278,.T.);
#5768=ORIENTED_EDGE('',*,*,#4279,.T.);
#5769=ORIENTED_EDGE('',*,*,#4275,.F.);
#5770=ORIENTED_EDGE('',*,*,#4280,.T.);
#5771=ORIENTED_EDGE('',*,*,#4281,.T.);
#5772=ORIENTED_EDGE('',*,*,#4282,.T.);
#5773=ORIENTED_EDGE('',*,*,#4278,.F.);
#5774=ORIENTED_EDGE('',*,*,#4283,.T.);
#5775=ORIENTED_EDGE('',*,*,#4270,.T.);
#5776=ORIENTED_EDGE('',*,*,#4284,.T.);
#5777=ORIENTED_EDGE('',*,*,#4281,.F.);
#5778=ORIENTED_EDGE('',*,*,#4283,.F.);
#5779=ORIENTED_EDGE('',*,*,#4280,.F.);
#5780=ORIENTED_EDGE('',*,*,#4277,.F.);
#5781=ORIENTED_EDGE('',*,*,#4274,.F.);
#5782=ORIENTED_EDGE('',*,*,#4271,.F.);
#5783=ORIENTED_EDGE('',*,*,#4267,.F.);
#5784=ORIENTED_EDGE('',*,*,#4284,.F.);
#5785=ORIENTED_EDGE('',*,*,#4269,.F.);
#5786=ORIENTED_EDGE('',*,*,#4273,.F.);
#5787=ORIENTED_EDGE('',*,*,#4276,.F.);
#5788=ORIENTED_EDGE('',*,*,#4279,.F.);
#5789=ORIENTED_EDGE('',*,*,#4282,.F.);
#6008=CYLINDRICAL_SURFACE('',#7537,0.35);
#6009=CYLINDRICAL_SURFACE('',#7545,0.1954);
#6356=ADVANCED_FACE('',(#1238),#874,.T.);
#6357=ADVANCED_FACE('',(#1239),#326,.T.);
#6358=ADVANCED_FACE('',(#1240),#6008,.T.);
#6359=ADVANCED_FACE('',(#1241),#327,.T.);
#6360=ADVANCED_FACE('',(#1242,#666),#875,.T.);
#6361=ADVANCED_FACE('',(#1243),#328,.T.);
#6362=ADVANCED_FACE('',(#1244),#6009,.T.);
#6363=ADVANCED_FACE('',(#1245),#329,.T.);
#6364=ADVANCED_FACE('',(#1246),#876,.T.);
#6365=ADVANCED_FACE('',(#1247),#877,.F.);
#6366=ADVANCED_FACE('',(#1248),#878,.F.);
#6367=ADVANCED_FACE('',(#1249),#879,.F.);
#6368=ADVANCED_FACE('',(#1250),#880,.F.);
#6369=ADVANCED_FACE('',(#1251),#881,.F.);
#6370=ADVANCED_FACE('',(#1252),#882,.F.);
#6371=ADVANCED_FACE('',(#1253),#883,.F.);
#6372=ADVANCED_FACE('',(#1254),#884,.F.);
#6440=CLOSED_SHELL('',(#6356,#6357,#6358,#6359,#6360,#6361,#6362,#6363,
#6364));
#6441=CLOSED_SHELL('',(#6365,#6366,#6367,#6368,#6369,#6370,#6371,#6372));
#7532=AXIS2_PLACEMENT_3D('',#12942,#9409,#9410);
#7533=AXIS2_PLACEMENT_3D('',#12943,#9411,#9412);
#7534=AXIS2_PLACEMENT_3D('',#12945,#9413,#9414);
#7535=AXIS2_PLACEMENT_3D('',#12946,#9415,#9416);
#7536=AXIS2_PLACEMENT_3D('',#12948,#9417,#9418);
#7537=AXIS2_PLACEMENT_3D('',#12950,#9420,#9421);
#7538=AXIS2_PLACEMENT_3D('',#12952,#9422,#9423);
#7539=AXIS2_PLACEMENT_3D('',#12954,#9425,#9426);
#7540=AXIS2_PLACEMENT_3D('',#12956,#9427,#9428);
#7541=AXIS2_PLACEMENT_3D('',#12958,#9430,#9431);
#7542=AXIS2_PLACEMENT_3D('',#12960,#9432,#9433);
#7543=AXIS2_PLACEMENT_3D('',#12961,#9434,#9435);
#7544=AXIS2_PLACEMENT_3D('',#12963,#9436,#9437);
#7545=AXIS2_PLACEMENT_3D('',#12965,#9439,#9440);
#7546=AXIS2_PLACEMENT_3D('',#12967,#9441,#9442);
#7547=AXIS2_PLACEMENT_3D('',#12969,#9444,#9445);
#7548=AXIS2_PLACEMENT_3D('',#12971,#9446,#9447);
#7549=AXIS2_PLACEMENT_3D('',#12973,#9449,#9450);
#7550=AXIS2_PLACEMENT_3D('',#12974,#9451,#9452);
#7551=AXIS2_PLACEMENT_3D('',#12983,#9457,#9458);
#7552=AXIS2_PLACEMENT_3D('',#12989,#9462,#9463);
#7553=AXIS2_PLACEMENT_3D('',#12995,#9467,#9468);
#7554=AXIS2_PLACEMENT_3D('',#13001,#9472,#9473);
#7555=AXIS2_PLACEMENT_3D('',#13007,#9477,#9478);
#7556=AXIS2_PLACEMENT_3D('',#13010,#9481,#9482);
#7557=AXIS2_PLACEMENT_3D('',#13011,#9483,#9484);
#9409=DIRECTION('axis',(0.,0.,1.));
#9410=DIRECTION('refdir',(1.,0.,0.));
#9411=DIRECTION('center_axis',(0.,1.,0.));
#9412=DIRECTION('ref_axis',(0.,0.,1.));
#9413=DIRECTION('center_axis',(0.,-1.,0.));
#9414=DIRECTION('ref_axis',(1.,0.,0.));
#9415=DIRECTION('center_axis',(0.,-1.,0.));
#9416=DIRECTION('ref_axis',(1.,0.,0.));
#9417=DIRECTION('center_axis',(0.,-1.,0.));
#9418=DIRECTION('ref_axis',(1.,0.,0.));
#9419=DIRECTION('',(0.707106781186547,0.707106781186548,8.65956056235493E-17));
#9420=DIRECTION('center_axis',(0.,-1.,0.));
#9421=DIRECTION('ref_axis',(1.,0.,0.));
#9422=DIRECTION('center_axis',(0.,-1.,0.));
#9423=DIRECTION('ref_axis',(1.,0.,0.));
#9424=DIRECTION('',(0.,1.,0.));
#9425=DIRECTION('center_axis',(0.,1.,0.));
#9426=DIRECTION('ref_axis',(1.,0.,0.));
#9427=DIRECTION('center_axis',(0.,-1.,0.));
#9428=DIRECTION('ref_axis',(1.,0.,0.));
#9429=DIRECTION('',(-0.707106781186547,0.707106781186548,-8.65956056235493E-17));
#9430=DIRECTION('center_axis',(0.,-1.,0.));
#9431=DIRECTION('ref_axis',(0.,0.,-1.));
#9432=DIRECTION('center_axis',(0.,-1.,0.));
#9433=DIRECTION('ref_axis',(1.,0.,0.));
#9434=DIRECTION('center_axis',(0.,1.,0.));
#9435=DIRECTION('ref_axis',(1.,0.,0.));
#9436=DIRECTION('center_axis',(0.,1.,0.));
#9437=DIRECTION('ref_axis',(1.,0.,0.));
#9438=DIRECTION('',(-0.447213595499958,0.894427190999916,-5.47678698264203E-17));
#9439=DIRECTION('center_axis',(0.,-1.,0.));
#9440=DIRECTION('ref_axis',(1.,0.,0.));
#9441=DIRECTION('center_axis',(0.,1.,0.));
#9442=DIRECTION('ref_axis',(1.,0.,0.));
#9443=DIRECTION('',(0.,1.,0.));
#9444=DIRECTION('center_axis',(0.,1.,0.));
#9445=DIRECTION('ref_axis',(1.,0.,0.));
#9446=DIRECTION('center_axis',(0.,-1.,0.));
#9447=DIRECTION('ref_axis',(1.,0.,0.));
#9448=DIRECTION('',(-0.707106781186547,0.707106781186548,-8.65956056235493E-17));
#9449=DIRECTION('center_axis',(0.,-1.,0.));
#9450=DIRECTION('ref_axis',(0.,0.,-1.));
#9451=DIRECTION('center_axis',(0.866025403784439,0.,-0.5));
#9452=DIRECTION('ref_axis',(0.5,0.,0.866025403784439));
#9453=DIRECTION('',(-0.5,0.,-0.866025403784439));
#9454=DIRECTION('',(0.,-1.,0.));
#9455=DIRECTION('',(0.5,0.,0.866025403784439));
#9456=DIRECTION('',(0.,-1.,0.));
#9457=DIRECTION('center_axis',(1.60246890531964E-16,0.,-1.));
#9458=DIRECTION('ref_axis',(1.,0.,1.60246890531964E-16));
#9459=DIRECTION('',(-1.,0.,-1.60246890531964E-16));
#9460=DIRECTION('',(0.,-1.,0.));
#9461=DIRECTION('',(1.,0.,1.60246890531964E-16));
#9462=DIRECTION('center_axis',(-0.866025403784439,0.,-0.5));
#9463=DIRECTION('ref_axis',(0.5,0.,-0.866025403784439));
#9464=DIRECTION('',(-0.5,0.,0.866025403784439));
#9465=DIRECTION('',(0.,-1.,0.));
#9466=DIRECTION('',(0.5,0.,-0.866025403784439));
#9467=DIRECTION('center_axis',(-0.866025403784439,0.,0.5));
#9468=DIRECTION('ref_axis',(-0.5,0.,-0.866025403784439));
#9469=DIRECTION('',(0.5,0.,0.866025403784439));
#9470=DIRECTION('',(0.,-1.,0.));
#9471=DIRECTION('',(-0.5,0.,-0.866025403784439));
#9472=DIRECTION('center_axis',(-1.60246890531964E-16,0.,1.));
#9473=DIRECTION('ref_axis',(-1.,0.,-1.60246890531964E-16));
#9474=DIRECTION('',(1.,0.,1.60246890531964E-16));
#9475=DIRECTION('',(0.,-1.,0.));
#9476=DIRECTION('',(-1.,0.,-1.60246890531964E-16));
#9477=DIRECTION('center_axis',(0.866025403784439,0.,0.5));
#9478=DIRECTION('ref_axis',(-0.5,0.,0.866025403784439));
#9479=DIRECTION('',(0.5,0.,-0.866025403784439));
#9480=DIRECTION('',(-0.5,0.,0.866025403784439));
#9481=DIRECTION('center_axis',(0.,1.,0.));
#9482=DIRECTION('ref_axis',(1.,0.,0.));
#9483=DIRECTION('center_axis',(0.,-1.,0.));
#9484=DIRECTION('ref_axis',(0.,0.,-1.));
#12942=CARTESIAN_POINT('',(0.,0.,0.));
#12943=CARTESIAN_POINT('Origin',(0.3,0.4,0.));
#12944=CARTESIAN_POINT('',(-0.3,0.4,-3.67394039744206E-17));
#12945=CARTESIAN_POINT('Origin',(0.,0.4,0.));
#12946=CARTESIAN_POINT('Origin',(0.,0.375,0.));
#12947=CARTESIAN_POINT('',(-0.35,0.35,-4.28626379701573E-17));
#12948=CARTESIAN_POINT('Origin',(0.,0.35,0.));
#12949=CARTESIAN_POINT('',(-0.325,0.375,-3.9801020972289E-17));
#12950=CARTESIAN_POINT('Origin',(0.,0.19,0.));
#12951=CARTESIAN_POINT('',(-0.35,0.03,-4.28626379701574E-17));
#12952=CARTESIAN_POINT('Origin',(0.,0.03,0.));
#12953=CARTESIAN_POINT('',(-0.35,0.19,-4.28626379701574E-17));
#12954=CARTESIAN_POINT('Origin',(0.,0.0149999999999999,0.));
#12955=CARTESIAN_POINT('',(-0.32,-3.29597460435593E-17,-3.91886975727153E-17));
#12956=CARTESIAN_POINT('Origin',(0.,0.,0.));
#12957=CARTESIAN_POINT('',(-0.335,0.0149999999999999,-4.10256677714363E-17));
#12958=CARTESIAN_POINT('Origin',(0.22,0.,0.));
#12959=CARTESIAN_POINT('',(-0.22,-6.93889390390723E-18,-2.69422295812418E-17));
#12960=CARTESIAN_POINT('Origin',(0.,0.,0.));
#12961=CARTESIAN_POINT('Origin',(0.,-0.02,0.));
#12962=CARTESIAN_POINT('',(-0.1954,-0.0492,2.39295984553393E-17));
#12963=CARTESIAN_POINT('Origin',(0.,-0.0492,0.));
#12964=CARTESIAN_POINT('',(-0.21,-0.02,-2.57175827820944E-17));
#12965=CARTESIAN_POINT('Origin',(0.,-0.8,0.));
#12966=CARTESIAN_POINT('',(-0.1954,-1.5646,2.39295984553393E-17));
#12967=CARTESIAN_POINT('Origin',(0.,-1.5646,0.));
#12968=CARTESIAN_POINT('',(-0.1954,-0.8,-2.39295984553393E-17));
#12969=CARTESIAN_POINT('Origin',(0.,-1.58,0.));
#12970=CARTESIAN_POINT('',(-0.16,-1.6,-1.95943487863577E-17));
#12971=CARTESIAN_POINT('Origin',(0.,-1.6,0.));
#12972=CARTESIAN_POINT('',(-0.18,-1.58,-2.20436423846524E-17));
#12973=CARTESIAN_POINT('Origin',(0.,-1.6,0.));
#12974=CARTESIAN_POINT('Origin',(0.0866025403784439,-0.4,-0.15));
#12975=CARTESIAN_POINT('',(0.173205080756888,-0.4,0.));
#12976=CARTESIAN_POINT('',(0.0866025403784439,-0.4,-0.15));
#12977=CARTESIAN_POINT('',(0.173205080756888,-0.4,0.));
#12978=CARTESIAN_POINT('',(0.0866025403784439,-0.64,-0.15));
#12979=CARTESIAN_POINT('',(0.0866025403784439,-0.4,-0.15));
#12980=CARTESIAN_POINT('',(0.173205080756888,-0.64,0.));
#12981=CARTESIAN_POINT('',(0.173205080756888,-0.64,0.));
#12982=CARTESIAN_POINT('',(0.173205080756888,-0.4,0.));
#12983=CARTESIAN_POINT('Origin',(-0.0866025403784438,-0.4,-0.15));
#12984=CARTESIAN_POINT('',(-0.0866025403784438,-0.4,-0.15));
#12985=CARTESIAN_POINT('',(0.0866025403784439,-0.4,-0.15));
#12986=CARTESIAN_POINT('',(-0.0866025403784438,-0.64,-0.15));
#12987=CARTESIAN_POINT('',(-0.0866025403784438,-0.4,-0.15));
#12988=CARTESIAN_POINT('',(0.0866025403784439,-0.64,-0.15));
#12989=CARTESIAN_POINT('Origin',(-0.173205080756888,-0.4,-2.77555756156289E-17));
#12990=CARTESIAN_POINT('',(-0.173205080756888,-0.4,-2.12115047744981E-17));
#12991=CARTESIAN_POINT('',(-0.0866025403784438,-0.4,-0.15));
#12992=CARTESIAN_POINT('',(-0.173205080756888,-0.64,-2.77555756156289E-17));
#12993=CARTESIAN_POINT('',(-0.173205080756888,-0.4,-2.12115047744981E-17));
#12994=CARTESIAN_POINT('',(-0.0866025403784438,-0.64,-0.15));
#12995=CARTESIAN_POINT('Origin',(-0.0866025403784439,-0.4,0.15));
#12996=CARTESIAN_POINT('',(-0.0866025403784439,-0.4,0.15));
#12997=CARTESIAN_POINT('',(-0.173205080756888,-0.4,-2.12115047744981E-17));
#12998=CARTESIAN_POINT('',(-0.0866025403784439,-0.64,0.15));
#12999=CARTESIAN_POINT('',(-0.0866025403784439,-0.4,0.15));
#13000=CARTESIAN_POINT('',(-0.173205080756888,-0.64,-2.12115047744981E-17));
#13001=CARTESIAN_POINT('Origin',(0.0866025403784439,-0.4,0.15));
#13002=CARTESIAN_POINT('',(0.0866025403784439,-0.4,0.15));
#13003=CARTESIAN_POINT('',(-0.0866025403784439,-0.4,0.15));
#13004=CARTESIAN_POINT('',(0.0866025403784439,-0.64,0.15));
#13005=CARTESIAN_POINT('',(0.0866025403784439,-0.4,0.15));
#13006=CARTESIAN_POINT('',(-0.0866025403784439,-0.64,0.15));
#13007=CARTESIAN_POINT('Origin',(0.173205080756888,-0.4,0.));
#13008=CARTESIAN_POINT('',(0.0866025403784439,-0.4,0.15));
#13009=CARTESIAN_POINT('',(0.0866025403784439,-0.64,0.15));
#13010=CARTESIAN_POINT('Origin',(0.,-0.4,-2.77555756156289E-17));
#13011=CARTESIAN_POINT('Origin',(0.,-0.64,-2.77555756156289E-17));
#13228=UNCERTAINTY_MEASURE_WITH_UNIT(LENGTH_MEASURE(0.001),#13278,
'DISTANCE_ACCURACY_VALUE',
'Maximum model space distance between geometric entities at asserted c
onnectivities');
#13233=UNCERTAINTY_MEASURE_WITH_UNIT(LENGTH_MEASURE(0.001),#13278,
'DISTANCE_ACCURACY_VALUE',
'Maximum model space distance between geometric entities at asserted c
onnectivities');
#13272=(
GEOMETRIC_REPRESENTATION_CONTEXT(3)
GLOBAL_UNCERTAINTY_ASSIGNED_CONTEXT((#13228))
GLOBAL_UNIT_ASSIGNED_CONTEXT((#13278,#13280,#13281))
REPRESENTATION_CONTEXT('','3D')
);
#13277=(
GEOMETRIC_REPRESENTATION_CONTEXT(3)
GLOBAL_UNCERTAINTY_ASSIGNED_CONTEXT((#13233))
GLOBAL_UNIT_ASSIGNED_CONTEXT((#13278,#13280,#13281))
REPRESENTATION_CONTEXT('','3D')
);
#13278=(
LENGTH_UNIT()
NAMED_UNIT(*)
SI_UNIT(.CENTI.,.METRE.)
);
#13280=(
NAMED_UNIT(*)
PLANE_ANGLE_UNIT()
SI_UNIT($,.RADIAN.)
);
#13281=(
NAMED_UNIT(*)
SI_UNIT($,.STERADIAN.)
SOLID_ANGLE_UNIT()
);
#13320=SHAPE_DEFINITION_REPRESENTATION(#13370,#13477);
#13370=PRODUCT_DEFINITION_SHAPE('',$,#13521);
#13477=SHAPE_REPRESENTATION('',(#7532),#13272);
#13482=PRODUCT_DEFINITION_CONTEXT('part definition',#13613,'design');
#13521=PRODUCT_DEFINITION('Cap Screw - M4x16','Cap Screw - M4x16',#13564,
#13482);
#13564=PRODUCT_DEFINITION_FORMATION('',$,#13653);
#13613=APPLICATION_CONTEXT(
'Core Data for Automotive Mechanical Design Process');
#13614=PRODUCT_CONTEXT('part definition',#13613,'mechanical');
#13653=PRODUCT('Cap Screw - M4x16','Cap Screw - M4x16',
'Cap Screw - M4x16',(#13614));
#13721=COLOUR_RGB('Black',0.12,0.14,0.17);
#13722=FILL_AREA_STYLE_COLOUR('',#13721);
#13723=FILL_AREA_STYLE('',(#13722));
#13724=SURFACE_STYLE_FILL_AREA(#13723);
#13725=SURFACE_SIDE_STYLE('',(#13724));
#13726=SURFACE_STYLE_USAGE(.BOTH.,#13725);
#13727=PRESENTATION_STYLE_ASSIGNMENT((#13726));
ENDSEC;
END-ISO-10303-21;
